ISO-10303-21;
HEADER;
/* Generated by software containing ST-Developer
 * from STEP Tools, Inc. (www.steptools.com) 
 */

FILE_DESCRIPTION(
/* description */ ('Lifting hook block with sheave'),
/* implementation_level */ '2;1');

FILE_NAME(
/* name */ 'Sheave cap (1).step',
/* time_stamp */ '2026-10-28T03:23:54-07:00',
/* author */ (''),
/* organization */ (''),
/* preprocessor_version */ 'ST-DEVELOPER v20.2',
/* originating_system */ 'Autodesk Translation Framework v15.17.0.0',
/* authorisation */ '');

FILE_SCHEMA (('AUTOMOTIVE_DESIGN { 1 0 10303 214 3 1 1 }'));
ENDSEC;

DATA;
#10=MECHANICAL_DESIGN_GEOMETRIC_PRESENTATION_REPRESENTATION('',(#370),#9391);
#310=SHAPE_REPRESENTATION_RELATIONSHIP('SRR','None',#9542,#340);
#340=ADVANCED_BREP_SHAPE_REPRESENTATION('',(#406),#9377);
#370=STYLED_ITEM('',(#9773),#406);
#406=MANIFOLD_SOLID_BREP('Body1',#4908);
#619=LINE('',#8441,#907);
#620=LINE('',#8447,#908);
#621=LINE('',#8453,#909);
#622=LINE('',#8459,#910);
#623=LINE('',#8465,#911);
#624=LINE('',#8473,#912);
#625=LINE('',#8478,#913);
#907=VECTOR('',#6926,0.225);
#908=VECTOR('',#6933,0.225);
#909=VECTOR('',#6940,0.225);
#910=VECTOR('',#6947,0.225);
#911=VECTOR('',#6954,2.34);
#912=VECTOR('',#6965,1.9);
#913=VECTOR('',#6970,3.);
#1074=CYLINDRICAL_SURFACE('',#5658,0.225);
#1075=CYLINDRICAL_SURFACE('',#5661,0.225);
#1076=CYLINDRICAL_SURFACE('',#5664,0.225);
#1077=CYLINDRICAL_SURFACE('',#5667,0.225);
#1078=CYLINDRICAL_SURFACE('',#5670,2.34);
#1079=CYLINDRICAL_SURFACE('',#5675,1.9);
#1080=CYLINDRICAL_SURFACE('',#5677,3.);
#1191=FACE_BOUND('',#1778,.T.);
#1192=FACE_BOUND('',#1782,.T.);
#1193=FACE_BOUND('',#1783,.T.);
#1194=FACE_BOUND('',#1784,.T.);
#1195=FACE_BOUND('',#1785,.T.);
#1196=FACE_BOUND('',#1786,.T.);
#1197=FACE_BOUND('',#1788,.T.);
#1198=FACE_BOUND('',#1789,.T.);
#1199=FACE_BOUND('',#1790,.T.);
#1200=FACE_BOUND('',#1791,.T.);
#1201=FACE_BOUND('',#1792,.T.);
#1399=FACE_OUTER_BOUND('',#1772,.T.);
#1400=FACE_OUTER_BOUND('',#1773,.T.);
#1401=FACE_OUTER_BOUND('',#1774,.T.);
#1402=FACE_OUTER_BOUND('',#1775,.T.);
#1403=FACE_OUTER_BOUND('',#1776,.T.);
#1404=FACE_OUTER_BOUND('',#1777,.T.);
#1405=FACE_OUTER_BOUND('',#1779,.T.);
#1406=FACE_OUTER_BOUND('',#1780,.T.);
#1407=FACE_OUTER_BOUND('',#1781,.T.);
#1408=FACE_OUTER_BOUND('',#1787,.T.);
#1772=EDGE_LOOP('',(#3992,#3993,#3994,#3995));
#1773=EDGE_LOOP('',(#3996,#3997,#3998,#3999));
#1774=EDGE_LOOP('',(#4000,#4001,#4002,#4003));
#1775=EDGE_LOOP('',(#4004,#4005,#4006,#4007));
#1776=EDGE_LOOP('',(#4008,#4009,#4010,#4011));
#1777=EDGE_LOOP('',(#4012));
#1778=EDGE_LOOP('',(#4013));
#1779=EDGE_LOOP('',(#4014,#4015,#4016,#4017));
#1780=EDGE_LOOP('',(#4018,#4019,#4020,#4021));
#1781=EDGE_LOOP('',(#4022));
#1782=EDGE_LOOP('',(#4023));
#1783=EDGE_LOOP('',(#4024));
#1784=EDGE_LOOP('',(#4025));
#1785=EDGE_LOOP('',(#4026));
#1786=EDGE_LOOP('',(#4027));
#1787=EDGE_LOOP('',(#4028));
#1788=EDGE_LOOP('',(#4029));
#1789=EDGE_LOOP('',(#4030));
#1790=EDGE_LOOP('',(#4031));
#1791=EDGE_LOOP('',(#4032));
#1792=EDGE_LOOP('',(#4033));
#2089=CIRCLE('',#5659,0.225);
#2090=CIRCLE('',#5660,0.225);
#2091=CIRCLE('',#5662,0.225);
#2092=CIRCLE('',#5663,0.225);
#2093=CIRCLE('',#5665,0.225);
#2094=CIRCLE('',#5666,0.225);
#2095=CIRCLE('',#5668,0.225);
#2096=CIRCLE('',#5669,0.225);
#2097=CIRCLE('',#5671,2.34);
#2098=CIRCLE('',#5672,2.34);
#2099=CIRCLE('',#5674,1.9);
#2100=CIRCLE('',#5676,1.9);
#2101=CIRCLE('',#5678,3.);
#2102=CIRCLE('',#5679,3.);
#2458=VERTEX_POINT('',#8438);
#2459=VERTEX_POINT('',#8440);
#2460=VERTEX_POINT('',#8444);
#2461=VERTEX_POINT('',#8446);
#2462=VERTEX_POINT('',#8450);
#2463=VERTEX_POINT('',#8452);
#2464=VERTEX_POINT('',#8456);
#2465=VERTEX_POINT('',#8458);
#2466=VERTEX_POINT('',#8462);
#2467=VERTEX_POINT('',#8464);
#2468=VERTEX_POINT('',#8468);
#2469=VERTEX_POINT('',#8471);
#2470=VERTEX_POINT('',#8475);
#2471=VERTEX_POINT('',#8477);
#3000=EDGE_CURVE('',#2458,#2458,#2089,.T.);
#3001=EDGE_CURVE('',#2458,#2459,#619,.T.);
#3002=EDGE_CURVE('',#2459,#2459,#2090,.T.);
#3003=EDGE_CURVE('',#2460,#2460,#2091,.T.);
#3004=EDGE_CURVE('',#2460,#2461,#620,.T.);
#3005=EDGE_CURVE('',#2461,#2461,#2092,.T.);
#3006=EDGE_CURVE('',#2462,#2462,#2093,.T.);
#3007=EDGE_CURVE('',#2462,#2463,#621,.T.);
#3008=EDGE_CURVE('',#2463,#2463,#2094,.T.);
#3009=EDGE_CURVE('',#2464,#2464,#2095,.T.);
#3010=EDGE_CURVE('',#2464,#2465,#622,.T.);
#3011=EDGE_CURVE('',#2465,#2465,#2096,.T.);
#3012=EDGE_CURVE('',#2466,#2466,#2097,.T.);
#3013=EDGE_CURVE('',#2466,#2467,#623,.T.);
#3014=EDGE_CURVE('',#2467,#2467,#2098,.T.);
#3015=EDGE_CURVE('',#2468,#2468,#2099,.T.);
#3016=EDGE_CURVE('',#2469,#2469,#2100,.T.);
#3017=EDGE_CURVE('',#2469,#2468,#624,.T.);
#3018=EDGE_CURVE('',#2470,#2470,#2101,.T.);
#3019=EDGE_CURVE('',#2470,#2471,#625,.T.);
#3020=EDGE_CURVE('',#2471,#2471,#2102,.T.);
#3992=ORIENTED_EDGE('',*,*,#3000,.F.);
#3993=ORIENTED_EDGE('',*,*,#3001,.T.);
#3994=ORIENTED_EDGE('',*,*,#3002,.F.);
#3995=ORIENTED_EDGE('',*,*,#3001,.F.);
#3996=ORIENTED_EDGE('',*,*,#3003,.F.);
#3997=ORIENTED_EDGE('',*,*,#3004,.T.);
#3998=ORIENTED_EDGE('',*,*,#3005,.F.);
#3999=ORIENTED_EDGE('',*,*,#3004,.F.);
#4000=ORIENTED_EDGE('',*,*,#3006,.F.);
#4001=ORIENTED_EDGE('',*,*,#3007,.T.);
#4002=ORIENTED_EDGE('',*,*,#3008,.F.);
#4003=ORIENTED_EDGE('',*,*,#3007,.F.);
#4004=ORIENTED_EDGE('',*,*,#3009,.F.);
#4005=ORIENTED_EDGE('',*,*,#3010,.T.);
#4006=ORIENTED_EDGE('',*,*,#3011,.F.);
#4007=ORIENTED_EDGE('',*,*,#3010,.F.);
#4008=ORIENTED_EDGE('',*,*,#3012,.F.);
#4009=ORIENTED_EDGE('',*,*,#3013,.T.);
#4010=ORIENTED_EDGE('',*,*,#3014,.T.);
#4011=ORIENTED_EDGE('',*,*,#3013,.F.);
#4012=ORIENTED_EDGE('',*,*,#3014,.F.);
#4013=ORIENTED_EDGE('',*,*,#3015,.F.);
#4014=ORIENTED_EDGE('',*,*,#3016,.F.);
#4015=ORIENTED_EDGE('',*,*,#3017,.T.);
#4016=ORIENTED_EDGE('',*,*,#3015,.T.);
#4017=ORIENTED_EDGE('',*,*,#3017,.F.);
#4018=ORIENTED_EDGE('',*,*,#3018,.F.);
#4019=ORIENTED_EDGE('',*,*,#3019,.T.);
#4020=ORIENTED_EDGE('',*,*,#3020,.T.);
#4021=ORIENTED_EDGE('',*,*,#3019,.F.);
#4022=ORIENTED_EDGE('',*,*,#3018,.T.);
#4023=ORIENTED_EDGE('',*,*,#3016,.T.);
#4024=ORIENTED_EDGE('',*,*,#3011,.T.);
#4025=ORIENTED_EDGE('',*,*,#3008,.T.);
#4026=ORIENTED_EDGE('',*,*,#3005,.T.);
#4027=ORIENTED_EDGE('',*,*,#3002,.T.);
#4028=ORIENTED_EDGE('',*,*,#3020,.F.);
#4029=ORIENTED_EDGE('',*,*,#3012,.T.);
#4030=ORIENTED_EDGE('',*,*,#3009,.T.);
#4031=ORIENTED_EDGE('',*,*,#3006,.T.);
#4032=ORIENTED_EDGE('',*,*,#3003,.T.);
#4033=ORIENTED_EDGE('',*,*,#3000,.T.);
#4544=PLANE('',#5673);
#4545=PLANE('',#5680);
#4546=PLANE('',#5681);
#4775=ADVANCED_FACE('',(#1399),#1074,.F.);
#4776=ADVANCED_FACE('',(#1400),#1075,.F.);
#4777=ADVANCED_FACE('',(#1401),#1076,.F.);
#4778=ADVANCED_FACE('',(#1402),#1077,.F.);
#4779=ADVANCED_FACE('',(#1403),#1078,.T.);
#4780=ADVANCED_FACE('',(#1404,#1191),#4544,.F.);
#4781=ADVANCED_FACE('',(#1405),#1079,.F.);
#4782=ADVANCED_FACE('',(#1406),#1080,.T.);
#4783=ADVANCED_FACE('',(#1407,#1192,#1193,#1194,#1195,#1196),#4545,.T.);
#4784=ADVANCED_FACE('',(#1408,#1197,#1198,#1199,#1200,#1201),#4546,.F.);
#4908=CLOSED_SHELL('',(#4775,#4776,#4777,#4778,#4779,#4780,#4781,#4782,
#4783,#4784));
#5657=AXIS2_PLACEMENT_3D('',#8436,#6920,#6921);
#5658=AXIS2_PLACEMENT_3D('',#8437,#6922,#6923);
#5659=AXIS2_PLACEMENT_3D('',#8439,#6924,#6925);
#5660=AXIS2_PLACEMENT_3D('',#8442,#6927,#6928);
#5661=AXIS2_PLACEMENT_3D('',#8443,#6929,#6930);
#5662=AXIS2_PLACEMENT_3D('',#8445,#6931,#6932);
#5663=AXIS2_PLACEMENT_3D('',#8448,#6934,#6935);
#5664=AXIS2_PLACEMENT_3D('',#8449,#6936,#6937);
#5665=AXIS2_PLACEMENT_3D('',#8451,#6938,#6939);
#5666=AXIS2_PLACEMENT_3D('',#8454,#6941,#6942);
#5667=AXIS2_PLACEMENT_3D('',#8455,#6943,#6944);
#5668=AXIS2_PLACEMENT_3D('',#8457,#6945,#6946);
#5669=AXIS2_PLACEMENT_3D('',#8460,#6948,#6949);
#5670=AXIS2_PLACEMENT_3D('',#8461,#6950,#6951);
#5671=AXIS2_PLACEMENT_3D('',#8463,#6952,#6953);
#5672=AXIS2_PLACEMENT_3D('',#8466,#6955,#6956);
#5673=AXIS2_PLACEMENT_3D('',#8467,#6957,#6958);
#5674=AXIS2_PLACEMENT_3D('',#8469,#6959,#6960);
#5675=AXIS2_PLACEMENT_3D('',#8470,#6961,#6962);
#5676=AXIS2_PLACEMENT_3D('',#8472,#6963,#6964);
#5677=AXIS2_PLACEMENT_3D('',#8474,#6966,#6967);
#5678=AXIS2_PLACEMENT_3D('',#8476,#6968,#6969);
#5679=AXIS2_PLACEMENT_3D('',#8479,#6971,#6972);
#5680=AXIS2_PLACEMENT_3D('',#8480,#6973,#6974);
#5681=AXIS2_PLACEMENT_3D('',#8481,#6975,#6976);
#6920=DIRECTION('axis',(0.,0.,1.));
#6921=DIRECTION('refdir',(1.,0.,0.));
#6922=DIRECTION('center_axis',(0.,1.,0.));
#6923=DIRECTION('ref_axis',(1.,0.,0.));
#6924=DIRECTION('center_axis',(0.,1.,0.));
#6925=DIRECTION('ref_axis',(1.,0.,0.));
#6926=DIRECTION('',(0.,1.,0.));
#6927=DIRECTION('center_axis',(0.,-1.,0.));
#6928=DIRECTION('ref_axis',(1.,0.,0.));
#6929=DIRECTION('center_axis',(0.,1.,0.));
#6930=DIRECTION('ref_axis',(1.,0.,0.));
#6931=DIRECTION('center_axis',(0.,1.,0.));
#6932=DIRECTION('ref_axis',(1.,0.,0.));
#6933=DIRECTION('',(0.,1.,0.));
#6934=DIRECTION('center_axis',(0.,-1.,0.));
#6935=DIRECTION('ref_axis',(1.,0.,0.));
#6936=DIRECTION('center_axis',(0.,1.,0.));
#6937=DIRECTION('ref_axis',(1.,0.,0.));
#6938=DIRECTION('center_axis',(0.,1.,0.));
#6939=DIRECTION('ref_axis',(1.,0.,0.));
#6940=DIRECTION('',(0.,1.,0.));
#6941=DIRECTION('center_axis',(0.,-1.,0.));
#6942=DIRECTION('ref_axis',(1.,0.,0.));
#6943=DIRECTION('center_axis',(0.,1.,0.));
#6944=DIRECTION('ref_axis',(1.,0.,0.));
#6945=DIRECTION('center_axis',(0.,1.,0.));
#6946=DIRECTION('ref_axis',(1.,0.,0.));
#6947=DIRECTION('',(0.,1.,0.));
#6948=DIRECTION('center_axis',(0.,-1.,0.));
#6949=DIRECTION('ref_axis',(1.,0.,0.));
#6950=DIRECTION('center_axis',(0.,1.,0.));
#6951=DIRECTION('ref_axis',(1.,0.,0.));
#6952=DIRECTION('center_axis',(0.,1.,0.));
#6953=DIRECTION('ref_axis',(1.,0.,0.));
#6954=DIRECTION('',(0.,-1.,0.));
#6955=DIRECTION('center_axis',(0.,1.,0.));
#6956=DIRECTION('ref_axis',(1.,0.,0.));
#6957=DIRECTION('center_axis',(0.,1.,0.));
#6958=DIRECTION('ref_axis',(1.,0.,0.));
#6959=DIRECTION('center_axis',(0.,-1.,0.));
#6960=DIRECTION('ref_axis',(1.,0.,0.));
#6961=DIRECTION('center_axis',(0.,1.,0.));
#6962=DIRECTION('ref_axis',(1.,0.,0.));
#6963=DIRECTION('center_axis',(0.,-1.,0.));
#6964=DIRECTION('ref_axis',(1.,0.,0.));
#6965=DIRECTION('',(0.,-1.,0.));
#6966=DIRECTION('center_axis',(0.,1.,0.));
#6967=DIRECTION('ref_axis',(1.,0.,0.));
#6968=DIRECTION('center_axis',(0.,1.,0.));
#6969=DIRECTION('ref_axis',(1.,0.,0.));
#6970=DIRECTION('',(0.,-1.,0.));
#6971=DIRECTION('center_axis',(0.,1.,0.));
#6972=DIRECTION('ref_axis',(1.,0.,0.));
#6973=DIRECTION('center_axis',(0.,1.,0.));
#6974=DIRECTION('ref_axis',(1.,0.,0.));
#6975=DIRECTION('center_axis',(0.,1.,0.));
#6976=DIRECTION('ref_axis',(1.,0.,0.));
#8436=CARTESIAN_POINT('',(0.,0.,0.));
#8437=CARTESIAN_POINT('Origin',(-1.90918830920368,1.9,10.0908116907963));
#8438=CARTESIAN_POINT('',(-2.13418830920368,2.,10.0908116907963));
#8439=CARTESIAN_POINT('Origin',(-1.90918830920368,2.,10.0908116907963));
#8440=CARTESIAN_POINT('',(-2.13418830920368,2.3,10.0908116907963));
#8441=CARTESIAN_POINT('',(-2.13418830920368,1.9,10.0908116907963));
#8442=CARTESIAN_POINT('Origin',(-1.90918830920368,2.3,10.0908116907963));
#8443=CARTESIAN_POINT('Origin',(-1.90918830920368,1.9,13.9091883092037));
#8444=CARTESIAN_POINT('',(-2.13418830920368,2.,13.9091883092037));
#8445=CARTESIAN_POINT('Origin',(-1.90918830920368,2.,13.9091883092037));
#8446=CARTESIAN_POINT('',(-2.13418830920368,2.3,13.9091883092037));
#8447=CARTESIAN_POINT('',(-2.13418830920368,1.9,13.9091883092037));
#8448=CARTESIAN_POINT('Origin',(-1.90918830920368,2.3,13.9091883092037));
#8449=CARTESIAN_POINT('Origin',(1.90918830920368,1.9,13.9091883092037));
#8450=CARTESIAN_POINT('',(1.68418830920368,2.,13.9091883092037));
#8451=CARTESIAN_POINT('Origin',(1.90918830920368,2.,13.9091883092037));
#8452=CARTESIAN_POINT('',(1.68418830920368,2.3,13.9091883092037));
#8453=CARTESIAN_POINT('',(1.68418830920368,1.9,13.9091883092037));
#8454=CARTESIAN_POINT('Origin',(1.90918830920368,2.3,13.9091883092037));
#8455=CARTESIAN_POINT('Origin',(1.90918830920368,1.9,10.0908116907963));
#8456=CARTESIAN_POINT('',(1.68418830920368,2.,10.0908116907963));
#8457=CARTESIAN_POINT('Origin',(1.90918830920368,2.,10.0908116907963));
#8458=CARTESIAN_POINT('',(1.68418830920368,2.3,10.0908116907963));
#8459=CARTESIAN_POINT('',(1.68418830920368,1.9,10.0908116907963));
#8460=CARTESIAN_POINT('Origin',(1.90918830920368,2.3,10.0908116907963));
#8461=CARTESIAN_POINT('Origin',(0.,1.7,12.));
#8462=CARTESIAN_POINT('',(-2.34,2.,12.));
#8463=CARTESIAN_POINT('Origin',(0.,2.,12.));
#8464=CARTESIAN_POINT('',(-2.34,1.7,12.));
#8465=CARTESIAN_POINT('',(-2.34,1.7,12.));
#8466=CARTESIAN_POINT('Origin',(0.,1.7,12.));
#8467=CARTESIAN_POINT('Origin',(0.,1.7,12.));
#8468=CARTESIAN_POINT('',(-1.9,1.7,12.));
#8469=CARTESIAN_POINT('Origin',(0.,1.7,12.));
#8470=CARTESIAN_POINT('Origin',(0.,2.,12.));
#8471=CARTESIAN_POINT('',(-1.9,2.3,12.));
#8472=CARTESIAN_POINT('Origin',(0.,2.3,12.));
#8473=CARTESIAN_POINT('',(-1.9,2.,12.));
#8474=CARTESIAN_POINT('Origin',(0.,2.,12.));
#8475=CARTESIAN_POINT('',(-3.,2.3,12.));
#8476=CARTESIAN_POINT('Origin',(0.,2.3,12.));
#8477=CARTESIAN_POINT('',(-3.,2.,12.));
#8478=CARTESIAN_POINT('',(-3.,2.,12.));
#8479=CARTESIAN_POINT('Origin',(0.,2.,12.));
#8480=CARTESIAN_POINT('Origin',(0.,2.3,12.));
#8481=CARTESIAN_POINT('Origin',(0.,2.,12.));
#9340=UNCERTAINTY_MEASURE_WITH_UNIT(LENGTH_MEASURE(0.001),#9392,
'DISTANCE_ACCURACY_VALUE',
'Maximum model space distance between geometric entities at asserted c
onnectivities');
#9354=UNCERTAINTY_MEASURE_WITH_UNIT(LENGTH_MEASURE(0.001),#9392,
'DISTANCE_ACCURACY_VALUE',
'Maximum model space distance between geometric entities at asserted c
onnectivities');
#9377=(
GEOMETRIC_REPRESENTATION_CONTEXT(3)
GLOBAL_UNCERTAINTY_ASSIGNED_CONTEXT((#9340))
GLOBAL_UNIT_ASSIGNED_CONTEXT((#9392,#9394,#9395))
REPRESENTATION_CONTEXT('','3D')
);
#9391=(
GEOMETRIC_REPRESENTATION_CONTEXT(3)
GLOBAL_UNCERTAINTY_ASSIGNED_CONTEXT((#9354))
GLOBAL_UNIT_ASSIGNED_CONTEXT((#9392,#9394,#9395))
REPRESENTATION_CONTEXT('','3D')
);
#9392=(
LENGTH_UNIT()
NAMED_UNIT(*)
SI_UNIT(.CENTI.,.METRE.)
);
#9394=(
NAMED_UNIT(*)
PLANE_ANGLE_UNIT()
SI_UNIT($,.RADIAN.)
);
#9395=(
NAMED_UNIT(*)
SI_UNIT($,.STERADIAN.)
SOLID_ANGLE_UNIT()
);
#9418=SHAPE_DEFINITION_REPRESENTATION(#9479,#9542);
#9479=PRODUCT_DEFINITION_SHAPE('',$,#9579);
#9542=SHAPE_REPRESENTATION('',(#5657),#9377);
#9556=PRODUCT_DEFINITION_CONTEXT('part definition',#9666,'design');
#9579=PRODUCT_DEFINITION('Sheave cap (1)','Sheave cap (1)',#9615,#9556);
#9615=PRODUCT_DEFINITION_FORMATION('',$,#9690);
#9666=APPLICATION_CONTEXT(
'Core Data for Automotive Mechanical Design Process');
#9667=PRODUCT_CONTEXT('part definition',#9666,'mechanical');
#9690=PRODUCT('Sheave cap (1)','Sheave cap (1)','Sheave cap (1)',(#9667));
#9767=COLOUR_RGB('Off White',0.89,0.88,0.83);
#9768=FILL_AREA_STYLE_COLOUR('',#9767);
#9769=FILL_AREA_STYLE('',(#9768));
#9770=SURFACE_STYLE_FILL_AREA(#9769);
#9771=SURFACE_SIDE_STYLE('',(#9770));
#9772=SURFACE_STYLE_USAGE(.BOTH.,#9771);
#9773=PRESENTATION_STYLE_ASSIGNMENT((#9772));
ENDSEC;
END-ISO-10303-21;
